ISO-10303-21;
HEADER;
/* Generated by software containing ST-Developer
 * from STEP Tools, Inc. (www.steptools.com) 
 */

FILE_DESCRIPTION(
/* description */ ('Belt conveyor head drive unit'),
/* implementation_level */ '2;1');

FILE_NAME(
/* name */ 'M8x25 Bolt.step',
/* time_stamp */ '2026-10-28T03:26:19-07:00',
/* author */ (''),
/* organization */ (''),
/* preprocessor_version */ 'ST-DEVELOPER v20.2',
/* originating_system */ 'Autodesk Translation Framework v15.17.0.0',
/* authorisation */ '');

FILE_SCHEMA (('AUTOMOTIVE_DESIGN { 1 0 10303 214 3 1 1 }'));
ENDSEC;

DATA;
#10=MECHANICAL_DESIGN_GEOMETRIC_PRESENTATION_REPRESENTATION('',(#905),#27069);
#13=ORIENTED_CLOSED_SHELL('',*,#13772,.F.);
#18=BREP_WITH_VOIDS('Body1',#13773,(#13));
#693=CONICAL_SURFACE('',#15601,0.625,0.785398163397448);
#694=CONICAL_SURFACE('',#15605,0.635,0.785398163397449);
#695=CONICAL_SURFACE('',#15609,0.41,0.463647609000806);
#751=SHAPE_REPRESENTATION_RELATIONSHIP('SRR','None',#27398,#820);
#820=ADVANCED_BREP_SHAPE_REPRESENTATION('',(#18),#27040);
#905=STYLED_ITEM('',(#27804),#18);
#1203=FACE_BOUND('',#3120,.T.);
#1519=PLANE('',#15589);
#1520=PLANE('',#15590);
#1521=PLANE('',#15591);
#1522=PLANE('',#15592);
#1523=PLANE('',#15593);
#1524=PLANE('',#15594);
#1525=PLANE('',#15595);
#1526=PLANE('',#15596);
#1527=PLANE('',#15597);
#1528=PLANE('',#15599);
#1529=PLANE('',#15607);
#2115=FACE_OUTER_BOUND('',#3106,.T.);
#2116=FACE_OUTER_BOUND('',#3107,.T.);
#2117=FACE_OUTER_BOUND('',#3108,.T.);
#2118=FACE_OUTER_BOUND('',#3109,.T.);
#2119=FACE_OUTER_BOUND('',#3110,.T.);
#2120=FACE_OUTER_BOUND('',#3111,.T.);
#2121=FACE_OUTER_BOUND('',#3112,.T.);
#2122=FACE_OUTER_BOUND('',#3113,.T.);
#2123=FACE_OUTER_BOUND('',#3114,.T.);
#2124=FACE_OUTER_BOUND('',#3115,.T.);
#2125=FACE_OUTER_BOUND('',#3116,.T.);
#2126=FACE_OUTER_BOUND('',#3117,.T.);
#2127=FACE_OUTER_BOUND('',#3118,.T.);
#2128=FACE_OUTER_BOUND('',#3119,.T.);
#2129=FACE_OUTER_BOUND('',#3121,.T.);
#2130=FACE_OUTER_BOUND('',#3122,.T.);
#3106=EDGE_LOOP('',(#11040,#11041,#11042,#11043));
#3107=EDGE_LOOP('',(#11044,#11045,#11046,#11047));
#3108=EDGE_LOOP('',(#11048,#11049,#11050,#11051));
#3109=EDGE_LOOP('',(#11052,#11053,#11054,#11055));
#3110=EDGE_LOOP('',(#11056,#11057,#11058,#11059));
#3111=EDGE_LOOP('',(#11060,#11061,#11062,#11063));
#3112=EDGE_LOOP('',(#11064,#11065,#11066,#11067,#11068,#11069));
#3113=EDGE_LOOP('',(#11070,#11071,#11072,#11073,#11074,#11075));
#3114=EDGE_LOOP('',(#11076));
#3115=EDGE_LOOP('',(#11077));
#3116=EDGE_LOOP('',(#11078,#11079,#11080,#11081));
#3117=EDGE_LOOP('',(#11082,#11083,#11084,#11085));
#3118=EDGE_LOOP('',(#11086,#11087,#11088,#11089));
#3119=EDGE_LOOP('',(#11090));
#3120=EDGE_LOOP('',(#11091));
#3121=EDGE_LOOP('',(#11092,#11093,#11094,#11095));
#3122=EDGE_LOOP('',(#11096,#11097,#11098,#11099));
#3998=LINE('',#24312,#4790);
#3999=LINE('',#24314,#4791);
#4000=LINE('',#24316,#4792);
#4001=LINE('',#24317,#4793);
#4002=LINE('',#24320,#4794);
#4003=LINE('',#24322,#4795);
#4004=LINE('',#24323,#4796);
#4005=LINE('',#24326,#4797);
#4006=LINE('',#24328,#4798);
#4007=LINE('',#24329,#4799);
#4008=LINE('',#24332,#4800);
#4009=LINE('',#24334,#4801);
#4010=LINE('',#24335,#4802);
#4011=LINE('',#24338,#4803);
#4012=LINE('',#24340,#4804);
#4013=LINE('',#24341,#4805);
#4014=LINE('',#24343,#4806);
#4015=LINE('',#24344,#4807);
#4016=LINE('',#24356,#4808);
#4017=LINE('',#24360,#4809);
#4018=LINE('',#24364,#4810);
#4019=LINE('',#24371,#4811);
#4020=LINE('',#24373,#4812);
#4790=VECTOR('',#18990,1.);
#4791=VECTOR('',#18991,1.);
#4792=VECTOR('',#18992,1.);
#4793=VECTOR('',#18993,1.);
#4794=VECTOR('',#18996,1.);
#4795=VECTOR('',#18997,1.);
#4796=VECTOR('',#18998,1.);
#4797=VECTOR('',#19001,1.);
#4798=VECTOR('',#19002,1.);
#4799=VECTOR('',#19003,1.);
#4800=VECTOR('',#19006,1.);
#4801=VECTOR('',#19007,1.);
#4802=VECTOR('',#19008,1.);
#4803=VECTOR('',#19011,1.);
#4804=VECTOR('',#19012,1.);
#4805=VECTOR('',#19013,1.);
#4806=VECTOR('',#19016,1.);
#4807=VECTOR('',#19017,1.);
#4808=VECTOR('',#19034,0.625);
#4809=VECTOR('',#19039,0.65);
#4810=VECTOR('',#19044,0.635);
#4811=VECTOR('',#19053,0.41);
#4812=VECTOR('',#19056,0.4);
#5567=CIRCLE('',#15598,0.3933);
#5568=CIRCLE('',#15600,0.6);
#5569=CIRCLE('',#15602,0.65);
#5570=CIRCLE('',#15604,0.65);
#5571=CIRCLE('',#15606,0.62);
#5572=CIRCLE('',#15608,0.42);
#5573=CIRCLE('',#15610,0.3933);
#6669=VERTEX_POINT('',#24310);
#6670=VERTEX_POINT('',#24311);
#6671=VERTEX_POINT('',#24313);
#6672=VERTEX_POINT('',#24315);
#6673=VERTEX_POINT('',#24319);
#6674=VERTEX_POINT('',#24321);
#6675=VERTEX_POINT('',#24325);
#6676=VERTEX_POINT('',#24327);
#6677=VERTEX_POINT('',#24331);
#6678=VERTEX_POINT('',#24333);
#6679=VERTEX_POINT('',#24337);
#6680=VERTEX_POINT('',#24339);
#6681=VERTEX_POINT('',#24348);
#6682=VERTEX_POINT('',#24351);
#6683=VERTEX_POINT('',#24354);
#6684=VERTEX_POINT('',#24358);
#6685=VERTEX_POINT('',#24362);
#6686=VERTEX_POINT('',#24366);
#6687=VERTEX_POINT('',#24369);
#8212=EDGE_CURVE('',#6669,#6670,#3998,.T.);
#8213=EDGE_CURVE('',#6670,#6671,#3999,.T.);
#8214=EDGE_CURVE('',#6671,#6672,#4000,.T.);
#8215=EDGE_CURVE('',#6669,#6672,#4001,.T.);
#8216=EDGE_CURVE('',#6670,#6673,#4002,.T.);
#8217=EDGE_CURVE('',#6673,#6674,#4003,.T.);
#8218=EDGE_CURVE('',#6674,#6671,#4004,.T.);
#8219=EDGE_CURVE('',#6673,#6675,#4005,.T.);
#8220=EDGE_CURVE('',#6675,#6676,#4006,.T.);
#8221=EDGE_CURVE('',#6676,#6674,#4007,.T.);
#8222=EDGE_CURVE('',#6675,#6677,#4008,.T.);
#8223=EDGE_CURVE('',#6677,#6678,#4009,.T.);
#8224=EDGE_CURVE('',#6678,#6676,#4010,.T.);
#8225=EDGE_CURVE('',#6677,#6679,#4011,.T.);
#8226=EDGE_CURVE('',#6679,#6680,#4012,.T.);
#8227=EDGE_CURVE('',#6680,#6678,#4013,.T.);
#8228=EDGE_CURVE('',#6679,#6669,#4014,.T.);
#8229=EDGE_CURVE('',#6672,#6680,#4015,.T.);
#8230=EDGE_CURVE('',#6681,#6681,#5567,.T.);
#8231=EDGE_CURVE('',#6682,#6682,#5568,.T.);
#8232=EDGE_CURVE('',#6683,#6683,#5569,.T.);
#8233=EDGE_CURVE('',#6683,#6682,#4016,.T.);
#8234=EDGE_CURVE('',#6684,#6684,#5570,.T.);
#8235=EDGE_CURVE('',#6684,#6683,#4017,.T.);
#8236=EDGE_CURVE('',#6685,#6685,#5571,.T.);
#8237=EDGE_CURVE('',#6685,#6684,#4018,.T.);
#8238=EDGE_CURVE('',#6686,#6686,#5572,.T.);
#8239=EDGE_CURVE('',#6687,#6687,#5573,.F.);
#8240=EDGE_CURVE('',#6687,#6686,#4019,.T.);
#8241=EDGE_CURVE('',#6681,#6687,#4020,.T.);
#11040=ORIENTED_EDGE('',*,*,#8212,.T.);
#11041=ORIENTED_EDGE('',*,*,#8213,.T.);
#11042=ORIENTED_EDGE('',*,*,#8214,.T.);
#11043=ORIENTED_EDGE('',*,*,#8215,.F.);
#11044=ORIENTED_EDGE('',*,*,#8216,.T.);
#11045=ORIENTED_EDGE('',*,*,#8217,.T.);
#11046=ORIENTED_EDGE('',*,*,#8218,.T.);
#11047=ORIENTED_EDGE('',*,*,#8213,.F.);
#11048=ORIENTED_EDGE('',*,*,#8219,.T.);
#11049=ORIENTED_EDGE('',*,*,#8220,.T.);
#11050=ORIENTED_EDGE('',*,*,#8221,.T.);
#11051=ORIENTED_EDGE('',*,*,#8217,.F.);
#11052=ORIENTED_EDGE('',*,*,#8222,.T.);
#11053=ORIENTED_EDGE('',*,*,#8223,.T.);
#11054=ORIENTED_EDGE('',*,*,#8224,.T.);
#11055=ORIENTED_EDGE('',*,*,#8220,.F.);
#11056=ORIENTED_EDGE('',*,*,#8225,.T.);
#11057=ORIENTED_EDGE('',*,*,#8226,.T.);
#11058=ORIENTED_EDGE('',*,*,#8227,.T.);
#11059=ORIENTED_EDGE('',*,*,#8223,.F.);
#11060=ORIENTED_EDGE('',*,*,#8228,.T.);
#11061=ORIENTED_EDGE('',*,*,#8215,.T.);
#11062=ORIENTED_EDGE('',*,*,#8229,.T.);
#11063=ORIENTED_EDGE('',*,*,#8226,.F.);
#11064=ORIENTED_EDGE('',*,*,#8228,.F.);
#11065=ORIENTED_EDGE('',*,*,#8225,.F.);
#11066=ORIENTED_EDGE('',*,*,#8222,.F.);
#11067=ORIENTED_EDGE('',*,*,#8219,.F.);
#11068=ORIENTED_EDGE('',*,*,#8216,.F.);
#11069=ORIENTED_EDGE('',*,*,#8212,.F.);
#11070=ORIENTED_EDGE('',*,*,#8229,.F.);
#11071=ORIENTED_EDGE('',*,*,#8214,.F.);
#11072=ORIENTED_EDGE('',*,*,#8218,.F.);
#11073=ORIENTED_EDGE('',*,*,#8221,.F.);
#11074=ORIENTED_EDGE('',*,*,#8224,.F.);
#11075=ORIENTED_EDGE('',*,*,#8227,.F.);
#11076=ORIENTED_EDGE('',*,*,#8230,.F.);
#11077=ORIENTED_EDGE('',*,*,#8231,.F.);
#11078=ORIENTED_EDGE('',*,*,#8232,.F.);
#11079=ORIENTED_EDGE('',*,*,#8233,.T.);
#11080=ORIENTED_EDGE('',*,*,#8231,.T.);
#11081=ORIENTED_EDGE('',*,*,#8233,.F.);
#11082=ORIENTED_EDGE('',*,*,#8234,.F.);
#11083=ORIENTED_EDGE('',*,*,#8235,.T.);
#11084=ORIENTED_EDGE('',*,*,#8232,.T.);
#11085=ORIENTED_EDGE('',*,*,#8235,.F.);
#11086=ORIENTED_EDGE('',*,*,#8236,.F.);
#11087=ORIENTED_EDGE('',*,*,#8237,.T.);
#11088=ORIENTED_EDGE('',*,*,#8234,.T.);
#11089=ORIENTED_EDGE('',*,*,#8237,.F.);
#11090=ORIENTED_EDGE('',*,*,#8236,.T.);
#11091=ORIENTED_EDGE('',*,*,#8238,.F.);
#11092=ORIENTED_EDGE('',*,*,#8239,.F.);
#11093=ORIENTED_EDGE('',*,*,#8240,.T.);
#11094=ORIENTED_EDGE('',*,*,#8238,.T.);
#11095=ORIENTED_EDGE('',*,*,#8240,.F.);
#11096=ORIENTED_EDGE('',*,*,#8230,.T.);
#11097=ORIENTED_EDGE('',*,*,#8241,.T.);
#11098=ORIENTED_EDGE('',*,*,#8239,.T.);
#11099=ORIENTED_EDGE('',*,*,#8241,.F.);
#12720=CYLINDRICAL_SURFACE('',#15603,0.65);
#12721=CYLINDRICAL_SURFACE('',#15611,0.3933);
#13394=ADVANCED_FACE('',(#2115),#1519,.F.);
#13395=ADVANCED_FACE('',(#2116),#1520,.F.);
#13396=ADVANCED_FACE('',(#2117),#1521,.F.);
#13397=ADVANCED_FACE('',(#2118),#1522,.F.);
#13398=ADVANCED_FACE('',(#2119),#1523,.F.);
#13399=ADVANCED_FACE('',(#2120),#1524,.F.);
#13400=ADVANCED_FACE('',(#2121),#1525,.F.);
#13401=ADVANCED_FACE('',(#2122),#1526,.F.);
#13402=ADVANCED_FACE('',(#2123),#1527,.F.);
#13403=ADVANCED_FACE('',(#2124),#1528,.T.);
#13404=ADVANCED_FACE('',(#2125),#693,.T.);
#13405=ADVANCED_FACE('',(#2126),#12720,.T.);
#13406=ADVANCED_FACE('',(#2127),#694,.T.);
#13407=ADVANCED_FACE('',(#2128,#1203),#1529,.T.);
#13408=ADVANCED_FACE('',(#2129),#695,.T.);
#13409=ADVANCED_FACE('',(#2130),#12721,.T.);
#13772=CLOSED_SHELL('',(#13394,#13395,#13396,#13397,#13398,#13399,#13400,
#13401));
#13773=CLOSED_SHELL('',(#13402,#13403,#13404,#13405,#13406,#13407,#13408,
#13409));
#15588=AXIS2_PLACEMENT_3D('',#24308,#18986,#18987);
#15589=AXIS2_PLACEMENT_3D('',#24309,#18988,#18989);
#15590=AXIS2_PLACEMENT_3D('',#24318,#18994,#18995);
#15591=AXIS2_PLACEMENT_3D('',#24324,#18999,#19000);
#15592=AXIS2_PLACEMENT_3D('',#24330,#19004,#19005);
#15593=AXIS2_PLACEMENT_3D('',#24336,#19009,#19010);
#15594=AXIS2_PLACEMENT_3D('',#24342,#19014,#19015);
#15595=AXIS2_PLACEMENT_3D('',#24345,#19018,#19019);
#15596=AXIS2_PLACEMENT_3D('',#24346,#19020,#19021);
#15597=AXIS2_PLACEMENT_3D('',#24347,#19022,#19023);
#15598=AXIS2_PLACEMENT_3D('',#24349,#19024,#19025);
#15599=AXIS2_PLACEMENT_3D('',#24350,#19026,#19027);
#15600=AXIS2_PLACEMENT_3D('',#24352,#19028,#19029);
#15601=AXIS2_PLACEMENT_3D('',#24353,#19030,#19031);
#15602=AXIS2_PLACEMENT_3D('',#24355,#19032,#19033);
#15603=AXIS2_PLACEMENT_3D('',#24357,#19035,#19036);
#15604=AXIS2_PLACEMENT_3D('',#24359,#19037,#19038);
#15605=AXIS2_PLACEMENT_3D('',#24361,#19040,#19041);
#15606=AXIS2_PLACEMENT_3D('',#24363,#19042,#19043);
#15607=AXIS2_PLACEMENT_3D('',#24365,#19045,#19046);
#15608=AXIS2_PLACEMENT_3D('',#24367,#19047,#19048);
#15609=AXIS2_PLACEMENT_3D('',#24368,#19049,#19050);
#15610=AXIS2_PLACEMENT_3D('',#24370,#19051,#19052);
#15611=AXIS2_PLACEMENT_3D('',#24372,#19054,#19055);
#18986=DIRECTION('axis',(0.,0.,1.));
#18987=DIRECTION('refdir',(1.,0.,0.));
#18988=DIRECTION('center_axis',(0.866025403784439,0.,-0.5));
#18989=DIRECTION('ref_axis',(0.5,0.,0.866025403784439));
#18990=DIRECTION('',(-0.5,0.,-0.866025403784439));
#18991=DIRECTION('',(0.,-1.,0.));
#18992=DIRECTION('',(0.5,0.,0.866025403784439));
#18993=DIRECTION('',(0.,-1.,0.));
#18994=DIRECTION('center_axis',(1.60246890531964E-16,0.,-1.));
#18995=DIRECTION('ref_axis',(1.,0.,1.60246890531964E-16));
#18996=DIRECTION('',(-1.,0.,-1.60246890531964E-16));
#18997=DIRECTION('',(0.,-1.,0.));
#18998=DIRECTION('',(1.,0.,1.60246890531964E-16));
#18999=DIRECTION('center_axis',(-0.866025403784439,0.,-0.5));
#19000=DIRECTION('ref_axis',(0.5,0.,-0.866025403784439));
#19001=DIRECTION('',(-0.5,0.,0.866025403784439));
#19002=DIRECTION('',(0.,-1.,0.));
#19003=DIRECTION('',(0.5,0.,-0.866025403784439));
#19004=DIRECTION('center_axis',(-0.866025403784439,0.,0.5));
#19005=DIRECTION('ref_axis',(-0.5,0.,-0.866025403784439));
#19006=DIRECTION('',(0.5,0.,0.866025403784439));
#19007=DIRECTION('',(0.,-1.,0.));
#19008=DIRECTION('',(-0.5,0.,-0.866025403784439));
#19009=DIRECTION('center_axis',(-1.60246890531964E-16,0.,1.));
#19010=DIRECTION('ref_axis',(-1.,0.,-1.60246890531964E-16));
#19011=DIRECTION('',(1.,0.,1.60246890531964E-16));
#19012=DIRECTION('',(0.,-1.,0.));
#19013=DIRECTION('',(-1.,0.,-1.60246890531964E-16));
#19014=DIRECTION('center_axis',(0.866025403784439,0.,0.5));
#19015=DIRECTION('ref_axis',(-0.5,0.,0.866025403784439));
#19016=DIRECTION('',(0.5,0.,-0.866025403784439));
#19017=DIRECTION('',(-0.5,0.,0.866025403784439));
#19018=DIRECTION('center_axis',(0.,1.,0.));
#19019=DIRECTION('ref_axis',(1.,0.,0.));
#19020=DIRECTION('center_axis',(0.,-1.,0.));
#19021=DIRECTION('ref_axis',(0.,0.,-1.));
#19022=DIRECTION('center_axis',(0.,1.,0.));
#19023=DIRECTION('ref_axis',(1.,0.,0.));
#19024=DIRECTION('center_axis',(0.,1.,0.));
#19025=DIRECTION('ref_axis',(1.,0.,0.));
#19026=DIRECTION('center_axis',(0.,1.,0.));
#19027=DIRECTION('ref_axis',(0.,0.,1.));
#19028=DIRECTION('center_axis',(0.,-1.,0.));
#19029=DIRECTION('ref_axis',(1.,0.,0.));
#19030=DIRECTION('center_axis',(0.,-1.,0.));
#19031=DIRECTION('ref_axis',(1.,0.,0.));
#19032=DIRECTION('center_axis',(0.,-1.,0.));
#19033=DIRECTION('ref_axis',(1.,0.,0.));
#19034=DIRECTION('',(0.707106781186548,0.707106781186547,8.65956056235493E-17));
#19035=DIRECTION('center_axis',(0.,-1.,0.));
#19036=DIRECTION('ref_axis',(1.,0.,0.));
#19037=DIRECTION('center_axis',(0.,-1.,0.));
#19038=DIRECTION('ref_axis',(1.,0.,0.));
#19039=DIRECTION('',(0.,1.,0.));
#19040=DIRECTION('center_axis',(0.,1.,0.));
#19041=DIRECTION('ref_axis',(1.,0.,0.));
#19042=DIRECTION('center_axis',(0.,-1.,0.));
#19043=DIRECTION('ref_axis',(1.,0.,0.));
#19044=DIRECTION('',(-0.707106781186548,0.707106781186547,-8.65956056235494E-17));
#19045=DIRECTION('center_axis',(0.,-1.,0.));
#19046=DIRECTION('ref_axis',(0.,0.,-1.));
#19047=DIRECTION('center_axis',(0.,-1.,0.));
#19048=DIRECTION('ref_axis',(1.,0.,0.));
#19049=DIRECTION('center_axis',(0.,1.,0.));
#19050=DIRECTION('ref_axis',(1.,0.,0.));
#19051=DIRECTION('center_axis',(0.,1.,0.));
#19052=DIRECTION('ref_axis',(1.,0.,0.));
#19053=DIRECTION('',(-0.447213595499958,0.894427190999916,-5.47678698264203E-17));
#19054=DIRECTION('center_axis',(0.,-1.,0.));
#19055=DIRECTION('ref_axis',(1.,0.,0.));
#19056=DIRECTION('',(0.,1.,0.));
#24308=CARTESIAN_POINT('',(0.,0.,0.));
#24309=CARTESIAN_POINT('Origin',(0.173205080756888,-0.8,-0.3));
#24310=CARTESIAN_POINT('',(0.346410161513775,-0.8,0.));
#24311=CARTESIAN_POINT('',(0.173205080756888,-0.8,-0.3));
#24312=CARTESIAN_POINT('',(0.346410161513775,-0.8,0.));
#24313=CARTESIAN_POINT('',(0.173205080756888,-1.28,-0.3));
#24314=CARTESIAN_POINT('',(0.173205080756888,-0.8,-0.3));
#24315=CARTESIAN_POINT('',(0.346410161513775,-1.28,0.));
#24316=CARTESIAN_POINT('',(0.346410161513775,-1.28,0.));
#24317=CARTESIAN_POINT('',(0.346410161513775,-0.8,0.));
#24318=CARTESIAN_POINT('Origin',(-0.173205080756888,-0.8,-0.3));
#24319=CARTESIAN_POINT('',(-0.173205080756888,-0.8,-0.3));
#24320=CARTESIAN_POINT('',(0.173205080756888,-0.8,-0.3));
#24321=CARTESIAN_POINT('',(-0.173205080756888,-1.28,-0.3));
#24322=CARTESIAN_POINT('',(-0.173205080756888,-0.8,-0.3));
#24323=CARTESIAN_POINT('',(0.173205080756888,-1.28,-0.3));
#24324=CARTESIAN_POINT('Origin',(-0.346410161513775,-0.8,-5.55111512312578E-17));
#24325=CARTESIAN_POINT('',(-0.346410161513775,-0.8,-4.24230095489963E-17));
#24326=CARTESIAN_POINT('',(-0.173205080756888,-0.8,-0.3));
#24327=CARTESIAN_POINT('',(-0.346410161513775,-1.28,-5.55111512312578E-17));
#24328=CARTESIAN_POINT('',(-0.346410161513775,-0.8,-4.24230095489963E-17));
#24329=CARTESIAN_POINT('',(-0.173205080756888,-1.28,-0.3));
#24330=CARTESIAN_POINT('Origin',(-0.173205080756888,-0.8,0.3));
#24331=CARTESIAN_POINT('',(-0.173205080756888,-0.8,0.3));
#24332=CARTESIAN_POINT('',(-0.346410161513775,-0.8,-4.24230095489963E-17));
#24333=CARTESIAN_POINT('',(-0.173205080756888,-1.28,0.3));
#24334=CARTESIAN_POINT('',(-0.173205080756888,-0.8,0.3));
#24335=CARTESIAN_POINT('',(-0.346410161513775,-1.28,-4.24230095489963E-17));
#24336=CARTESIAN_POINT('Origin',(0.173205080756888,-0.8,0.3));
#24337=CARTESIAN_POINT('',(0.173205080756888,-0.8,0.3));
#24338=CARTESIAN_POINT('',(-0.173205080756888,-0.8,0.3));
#24339=CARTESIAN_POINT('',(0.173205080756888,-1.28,0.3));
#24340=CARTESIAN_POINT('',(0.173205080756888,-0.8,0.3));
#24341=CARTESIAN_POINT('',(-0.173205080756888,-1.28,0.3));
#24342=CARTESIAN_POINT('Origin',(0.346410161513775,-0.8,0.));
#24343=CARTESIAN_POINT('',(0.173205080756888,-0.8,0.3));
#24344=CARTESIAN_POINT('',(0.173205080756888,-1.28,0.3));
#24345=CARTESIAN_POINT('Origin',(0.,-0.8,-5.55111512312578E-17));
#24346=CARTESIAN_POINT('Origin',(0.,-1.28,-5.55111512312578E-17));
#24347=CARTESIAN_POINT('Origin',(0.,-2.5,0.));
#24348=CARTESIAN_POINT('',(-0.3933,-2.5,4.81653586104654E-17));
#24349=CARTESIAN_POINT('Origin',(0.,-2.5,0.));
#24350=CARTESIAN_POINT('Origin',(0.6,0.8,0.));
#24351=CARTESIAN_POINT('',(-0.6,0.8,-7.34788079488412E-17));
#24352=CARTESIAN_POINT('Origin',(0.,0.8,0.));
#24353=CARTESIAN_POINT('Origin',(0.,0.775,0.));
#24354=CARTESIAN_POINT('',(-0.65,0.75,-7.9602041944578E-17));
#24355=CARTESIAN_POINT('Origin',(0.,0.75,0.));
#24356=CARTESIAN_POINT('',(-0.625,0.775,-7.65404249467096E-17));
#24357=CARTESIAN_POINT('Origin',(0.,0.39,0.));
#24358=CARTESIAN_POINT('',(-0.65,0.0299999999999998,-7.9602041944578E-17));
#24359=CARTESIAN_POINT('Origin',(0.,0.0299999999999998,0.));
#24360=CARTESIAN_POINT('',(-0.65,0.39,-7.9602041944578E-17));
#24361=CARTESIAN_POINT('Origin',(0.,0.0150000000000001,0.));
#24362=CARTESIAN_POINT('',(-0.62,5.89805981832114E-17,-7.59281015471359E-17));
#24363=CARTESIAN_POINT('Origin',(0.,0.,0.));
#24364=CARTESIAN_POINT('',(-0.635,0.0150000000000001,-7.77650717458569E-17));
#24365=CARTESIAN_POINT('Origin',(0.42,0.,0.));
#24366=CARTESIAN_POINT('',(-0.42,-3.46944695195361E-18,-5.14351655641888E-17));
#24367=CARTESIAN_POINT('Origin',(0.,0.,0.));
#24368=CARTESIAN_POINT('Origin',(0.,-0.02,0.));
#24369=CARTESIAN_POINT('',(-0.3933,-0.0534000000000001,4.81653586104654E-17));
#24370=CARTESIAN_POINT('Origin',(0.,-0.0534000000000001,0.));
#24371=CARTESIAN_POINT('',(-0.41,-0.02,-5.02105187650415E-17));
#24372=CARTESIAN_POINT('Origin',(0.,-1.48,0.));
#24373=CARTESIAN_POINT('',(-0.3933,-1.48,-4.81653586104654E-17));
#26963=UNCERTAINTY_MEASURE_WITH_UNIT(LENGTH_MEASURE(0.001),#27070,
'DISTANCE_ACCURACY_VALUE',
'Maximum model space distance between geometric entities at asserted c
onnectivities');
#26992=UNCERTAINTY_MEASURE_WITH_UNIT(LENGTH_MEASURE(0.001),#27070,
'DISTANCE_ACCURACY_VALUE',
'Maximum model space distance between geometric entities at asserted c
onnectivities');
#27040=(
GEOMETRIC_REPRESENTATION_CONTEXT(3)
GLOBAL_UNCERTAINTY_ASSIGNED_CONTEXT((#26963))
GLOBAL_UNIT_ASSIGNED_CONTEXT((#27070,#27072,#27073))
REPRESENTATION_CONTEXT('','3D')
);
#27069=(
GEOMETRIC_REPRESENTATION_CONTEXT(3)
GLOBAL_UNCERTAINTY_ASSIGNED_CONTEXT((#26992))
GLOBAL_UNIT_ASSIGNED_CONTEXT((#27070,#27072,#27073))
REPRESENTATION_CONTEXT('','3D')
);
#27070=(
LENGTH_UNIT()
NAMED_UNIT(*)
SI_UNIT(.CENTI.,.METRE.)
);
#27072=(
NAMED_UNIT(*)
PLANE_ANGLE_UNIT()
SI_UNIT($,.RADIAN.)
);
#27073=(
NAMED_UNIT(*)
SI_UNIT($,.STERADIAN.)
SOLID_ANGLE_UNIT()
);
#27121=SHAPE_DEFINITION_REPRESENTATION(#27209,#27398);
#27209=PRODUCT_DEFINITION_SHAPE('',$,#27475);
#27398=SHAPE_REPRESENTATION('',(#15588),#27040);
#27427=PRODUCT_DEFINITION_CONTEXT('part definition',#27657,'design');
#27475=PRODUCT_DEFINITION('M8x25 Bolt','M8x25 Bolt',#27551,#27427);
#27551=PRODUCT_DEFINITION_FORMATION('',$,#27706);
#27657=APPLICATION_CONTEXT(
'Core Data for Automotive Mechanical Design Process');
#27658=PRODUCT_CONTEXT('part definition',#27657,'mechanical');
#27706=PRODUCT('M8x25 Bolt','M8x25 Bolt','M8x25 Bolt',(#27658));
#27798=COLOUR_RGB('Black',0.12,0.14,0.17);
#27799=FILL_AREA_STYLE_COLOUR('',#27798);
#27800=FILL_AREA_STYLE('',(#27799));
#27801=SURFACE_STYLE_FILL_AREA(#27800);
#27802=SURFACE_SIDE_STYLE('',(#27801));
#27803=SURFACE_STYLE_USAGE(.BOTH.,#27802);
#27804=PRESENTATION_STYLE_ASSIGNMENT((#27803));
ENDSEC;
END-ISO-10303-21;
